ISO-10303-21;
HEADER;
/* Generated by software containing ST-Developer
 * from STEP Tools, Inc. (www.steptools.com) 
 */

FILE_DESCRIPTION(
/* description */ ('Guided pneumatic stop gate'),
/* implementation_level */ '2;1');

FILE_NAME(
/* name */ 'Flat Washer - M5.step',
/* time_stamp */ '2026-10-27T21:43:45-07:00',
/* author */ (''),
/* organization */ (''),
/* preprocessor_version */ 'ST-DEVELOPER v20.2',
/* originating_system */ 'Autodesk Translation Framework v15.17.0.0',
/* authorisation */ '');

FILE_SCHEMA (('AUTOMOTIVE_DESIGN { 1 0 10303 214 3 1 1 }'));
ENDSEC;

DATA;
#10=MECHANICAL_DESIGN_GEOMETRIC_PRESENTATION_REPRESENTATION('',(#552),#14392);
#431=CONICAL_SURFACE('',#8799,0.275,0.785398163397449);
#468=SHAPE_REPRESENTATION_RELATIONSHIP('SRR','None',#14603,#510);
#510=ADVANCED_BREP_SHAPE_REPRESENTATION('',(#593),#14365);
#552=STYLED_ITEM('',(#14898),#593);
#593=MANIFOLD_SOLID_BREP('Body1',#7893);
#695=FACE_BOUND('',#1892,.T.);
#696=FACE_BOUND('',#1895,.T.);
#969=PLANE('',#8804);
#970=PLANE('',#8808);
#1334=FACE_OUTER_BOUND('',#1889,.T.);
#1335=FACE_OUTER_BOUND('',#1890,.T.);
#1336=FACE_OUTER_BOUND('',#1891,.T.);
#1337=FACE_OUTER_BOUND('',#1893,.T.);
#1338=FACE_OUTER_BOUND('',#1894,.T.);
#1889=EDGE_LOOP('',(#6156,#6157,#6158,#6159));
#1890=EDGE_LOOP('',(#6160,#6161,#6162,#6163));
#1891=EDGE_LOOP('',(#6164));
#1892=EDGE_LOOP('',(#6165));
#1893=EDGE_LOOP('',(#6166,#6167,#6168,#6169));
#1894=EDGE_LOOP('',(#6170));
#1895=EDGE_LOOP('',(#6171));
#2522=LINE('',#12849,#3067);
#2523=LINE('',#12853,#3068);
#2524=LINE('',#12860,#3069);
#3067=VECTOR('',#10459,0.275);
#3068=VECTOR('',#10464,0.265);
#3069=VECTOR('',#10473,0.5);
#3530=CIRCLE('',#8800,0.285);
#3531=CIRCLE('',#8801,0.265);
#3532=CIRCLE('',#8803,0.265);
#3533=CIRCLE('',#8805,0.5);
#3534=CIRCLE('',#8807,0.5);
#4003=VERTEX_POINT('',#12846);
#4004=VERTEX_POINT('',#12848);
#4005=VERTEX_POINT('',#12852);
#4006=VERTEX_POINT('',#12856);
#4007=VERTEX_POINT('',#12859);
#4776=EDGE_CURVE('',#4003,#4003,#3530,.T.);
#4777=EDGE_CURVE('',#4003,#4004,#2522,.T.);
#4778=EDGE_CURVE('',#4004,#4004,#3531,.T.);
#4779=EDGE_CURVE('',#4004,#4005,#2523,.T.);
#4780=EDGE_CURVE('',#4005,#4005,#3532,.T.);
#4781=EDGE_CURVE('',#4006,#4006,#3533,.T.);
#4782=EDGE_CURVE('',#4006,#4007,#2524,.T.);
#4783=EDGE_CURVE('',#4007,#4007,#3534,.T.);
#6156=ORIENTED_EDGE('',*,*,#4776,.T.);
#6157=ORIENTED_EDGE('',*,*,#4777,.T.);
#6158=ORIENTED_EDGE('',*,*,#4778,.T.);
#6159=ORIENTED_EDGE('',*,*,#4777,.F.);
#6160=ORIENTED_EDGE('',*,*,#4778,.F.);
#6161=ORIENTED_EDGE('',*,*,#4779,.T.);
#6162=ORIENTED_EDGE('',*,*,#4780,.T.);
#6163=ORIENTED_EDGE('',*,*,#4779,.F.);
#6164=ORIENTED_EDGE('',*,*,#4781,.T.);
#6165=ORIENTED_EDGE('',*,*,#4776,.F.);
#6166=ORIENTED_EDGE('',*,*,#4781,.F.);
#6167=ORIENTED_EDGE('',*,*,#4782,.T.);
#6168=ORIENTED_EDGE('',*,*,#4783,.T.);
#6169=ORIENTED_EDGE('',*,*,#4782,.F.);
#6170=ORIENTED_EDGE('',*,*,#4783,.F.);
#6171=ORIENTED_EDGE('',*,*,#4780,.F.);
#7312=CYLINDRICAL_SURFACE('',#8802,0.265);
#7313=CYLINDRICAL_SURFACE('',#8806,0.5);
#7616=ADVANCED_FACE('',(#1334),#431,.F.);
#7617=ADVANCED_FACE('',(#1335),#7312,.F.);
#7618=ADVANCED_FACE('',(#1336,#695),#969,.T.);
#7619=ADVANCED_FACE('',(#1337),#7313,.T.);
#7620=ADVANCED_FACE('',(#1338,#696),#970,.F.);
#7893=CLOSED_SHELL('',(#7616,#7617,#7618,#7619,#7620));
#8798=AXIS2_PLACEMENT_3D('',#12844,#10453,#10454);
#8799=AXIS2_PLACEMENT_3D('',#12845,#10455,#10456);
#8800=AXIS2_PLACEMENT_3D('',#12847,#10457,#10458);
#8801=AXIS2_PLACEMENT_3D('',#12850,#10460,#10461);
#8802=AXIS2_PLACEMENT_3D('',#12851,#10462,#10463);
#8803=AXIS2_PLACEMENT_3D('',#12854,#10465,#10466);
#8804=AXIS2_PLACEMENT_3D('',#12855,#10467,#10468);
#8805=AXIS2_PLACEMENT_3D('',#12857,#10469,#10470);
#8806=AXIS2_PLACEMENT_3D('',#12858,#10471,#10472);
#8807=AXIS2_PLACEMENT_3D('',#12861,#10474,#10475);
#8808=AXIS2_PLACEMENT_3D('',#12862,#10476,#10477);
#10453=DIRECTION('axis',(0.,0.,1.));
#10454=DIRECTION('refdir',(1.,0.,0.));
#10455=DIRECTION('center_axis',(0.,1.,0.));
#10456=DIRECTION('ref_axis',(1.,0.,0.));
#10457=DIRECTION('center_axis',(0.,1.,0.));
#10458=DIRECTION('ref_axis',(1.,0.,0.));
#10459=DIRECTION('',(0.707106781186548,-0.707106781186547,-8.65956056235494E-17));
#10460=DIRECTION('center_axis',(0.,-1.,0.));
#10461=DIRECTION('ref_axis',(1.,0.,0.));
#10462=DIRECTION('center_axis',(0.,1.,0.));
#10463=DIRECTION('ref_axis',(1.,0.,0.));
#10464=DIRECTION('',(0.,-1.,0.));
#10465=DIRECTION('center_axis',(0.,-1.,0.));
#10466=DIRECTION('ref_axis',(1.,0.,0.));
#10467=DIRECTION('center_axis',(0.,1.,0.));
#10468=DIRECTION('ref_axis',(1.,0.,0.));
#10469=DIRECTION('center_axis',(0.,1.,0.));
#10470=DIRECTION('ref_axis',(1.,0.,0.));
#10471=DIRECTION('center_axis',(0.,1.,0.));
#10472=DIRECTION('ref_axis',(1.,0.,0.));
#10473=DIRECTION('',(0.,-1.,0.));
#10474=DIRECTION('center_axis',(0.,1.,0.));
#10475=DIRECTION('ref_axis',(1.,0.,0.));
#10476=DIRECTION('center_axis',(0.,1.,0.));
#10477=DIRECTION('ref_axis',(1.,0.,0.));
#12844=CARTESIAN_POINT('',(0.,0.,0.));
#12845=CARTESIAN_POINT('Origin',(0.,0.09,0.));
#12846=CARTESIAN_POINT('',(-0.285,0.1,3.49024337756996E-17));
#12847=CARTESIAN_POINT('Origin',(0.,0.1,0.));
#12848=CARTESIAN_POINT('',(-0.265,0.08,-3.24531401774049E-17));
#12849=CARTESIAN_POINT('',(-0.275,0.09,3.36777869765522E-17));
#12850=CARTESIAN_POINT('Origin',(0.,0.08,0.));
#12851=CARTESIAN_POINT('Origin',(0.,0.,0.));
#12852=CARTESIAN_POINT('',(-0.265,0.,3.24531401774049E-17));
#12853=CARTESIAN_POINT('',(-0.265,0.,3.24531401774049E-17));
#12854=CARTESIAN_POINT('Origin',(0.,0.,0.));
#12855=CARTESIAN_POINT('Origin',(0.,0.1,0.));
#12856=CARTESIAN_POINT('',(-0.5,0.1,6.12323399573677E-17));
#12857=CARTESIAN_POINT('Origin',(0.,0.1,0.));
#12858=CARTESIAN_POINT('Origin',(0.,0.,0.));
#12859=CARTESIAN_POINT('',(-0.5,0.,6.12323399573677E-17));
#12860=CARTESIAN_POINT('',(-0.5,0.,6.12323399573677E-17));
#12861=CARTESIAN_POINT('Origin',(0.,0.,0.));
#12862=CARTESIAN_POINT('Origin',(0.,0.,0.));
#14317=UNCERTAINTY_MEASURE_WITH_UNIT(LENGTH_MEASURE(0.001),#14393,
'DISTANCE_ACCURACY_VALUE',
'Maximum model space distance between geometric entities at asserted c
onnectivities');
#14344=UNCERTAINTY_MEASURE_WITH_UNIT(LENGTH_MEASURE(0.001),#14393,
'DISTANCE_ACCURACY_VALUE',
'Maximum model space distance between geometric entities at asserted c
onnectivities');
#14365=(
GEOMETRIC_REPRESENTATION_CONTEXT(3)
GLOBAL_UNCERTAINTY_ASSIGNED_CONTEXT((#14317))
GLOBAL_UNIT_ASSIGNED_CONTEXT((#14393,#14395,#14396))
REPRESENTATION_CONTEXT('','3D')
);
#14392=(
GEOMETRIC_REPRESENTATION_CONTEXT(3)
GLOBAL_UNCERTAINTY_ASSIGNED_CONTEXT((#14344))
GLOBAL_UNIT_ASSIGNED_CONTEXT((#14393,#14395,#14396))
REPRESENTATION_CONTEXT('','3D')
);
#14393=(
LENGTH_UNIT()
NAMED_UNIT(*)
SI_UNIT(.CENTI.,.METRE.)
);
#14395=(
NAMED_UNIT(*)
PLANE_ANGLE_UNIT()
SI_UNIT($,.RADIAN.)
);
#14396=(
NAMED_UNIT(*)
SI_UNIT($,.STERADIAN.)
SOLID_ANGLE_UNIT()
);
#14417=SHAPE_DEFINITION_REPRESENTATION(#14466,#14603);
#14466=PRODUCT_DEFINITION_SHAPE('',$,#14651);
#14603=SHAPE_REPRESENTATION('',(#8798),#14365);
#14630=PRODUCT_DEFINITION_CONTEXT('part definition',#14773,'design');
#14651=PRODUCT_DEFINITION('Flat Washer - M5','Flat Washer - M5',#14698,
#14630);
#14698=PRODUCT_DEFINITION_FORMATION('',$,#14795);
#14773=APPLICATION_CONTEXT(
'Core Data for Automotive Mechanical Design Process');
#14774=PRODUCT_CONTEXT('part definition',#14773,'mechanical');
#14795=PRODUCT('Flat Washer - M5','Flat Washer - M5','Flat Washer - M5',
(#14774));
#14892=COLOUR_RGB('Black',0.12,0.14,0.17);
#14893=FILL_AREA_STYLE_COLOUR('',#14892);
#14894=FILL_AREA_STYLE('',(#14893));
#14895=SURFACE_STYLE_FILL_AREA(#14894);
#14896=SURFACE_SIDE_STYLE('',(#14895));
#14897=SURFACE_STYLE_USAGE(.BOTH.,#14896);
#14898=PRESENTATION_STYLE_ASSIGNMENT((#14897));
ENDSEC;
END-ISO-10303-21;
